ISO-10303-21;
HEADER;
/* Generated by software containing ST-Developer
 * from STEP Tools, Inc. (www.steptools.com) 
 */

FILE_DESCRIPTION(
/* description */ ('Rigid flange shaft coupling assembly'),
/* implementation_level */ '2;1');

FILE_NAME(
/* name */ 'Socket Set Screw - M5x8.step',
/* time_stamp */ '2026-10-27T10:47:16-07:00',
/* author */ (''),
/* organization */ (''),
/* preprocessor_version */ 'ST-DEVELOPER v20.2',
/* originating_system */ 'Autodesk Translation Framework v15.17.0.0',
/* authorisation */ '');

FILE_SCHEMA (('AUTOMOTIVE_DESIGN { 1 0 10303 214 3 1 1 }'));
ENDSEC;

DATA;
#10=MECHANICAL_DESIGN_GEOMETRIC_PRESENTATION_REPRESENTATION('',(#426),#9141);
#36=CONICAL_SURFACE('',#5600,0.235,0.785398163397448);
#37=CONICAL_SURFACE('',#5604,0.2125,0.785398163397448);
#369=SHAPE_REPRESENTATION_RELATIONSHIP('SRR','None',#9305,#397);
#397=ADVANCED_BREP_SHAPE_REPRESENTATION('',(#452),#9140);
#426=STYLED_ITEM('',(#9507),#452);
#452=MANIFOLD_SOLID_BREP('Body1',#4783);
#569=FACE_BOUND('',#1400,.T.);
#735=PLANE('',#5591);
#736=PLANE('',#5592);
#737=PLANE('',#5593);
#738=PLANE('',#5594);
#739=PLANE('',#5595);
#740=PLANE('',#5596);
#741=PLANE('',#5597);
#742=PLANE('',#5598);
#743=PLANE('',#5606);
#1004=FACE_OUTER_BOUND('',#1392,.T.);
#1005=FACE_OUTER_BOUND('',#1393,.T.);
#1006=FACE_OUTER_BOUND('',#1394,.T.);
#1007=FACE_OUTER_BOUND('',#1395,.T.);
#1008=FACE_OUTER_BOUND('',#1396,.T.);
#1009=FACE_OUTER_BOUND('',#1397,.T.);
#1010=FACE_OUTER_BOUND('',#1398,.T.);
#1011=FACE_OUTER_BOUND('',#1399,.T.);
#1012=FACE_OUTER_BOUND('',#1401,.T.);
#1013=FACE_OUTER_BOUND('',#1402,.T.);
#1014=FACE_OUTER_BOUND('',#1403,.T.);
#1015=FACE_OUTER_BOUND('',#1404,.T.);
#1392=EDGE_LOOP('',(#4349,#4350,#4351,#4352));
#1393=EDGE_LOOP('',(#4353,#4354,#4355,#4356));
#1394=EDGE_LOOP('',(#4357,#4358,#4359,#4360));
#1395=EDGE_LOOP('',(#4361,#4362,#4363,#4364));
#1396=EDGE_LOOP('',(#4365,#4366,#4367,#4368));
#1397=EDGE_LOOP('',(#4369,#4370,#4371,#4372));
#1398=EDGE_LOOP('',(#4373,#4374,#4375,#4376,#4377,#4378));
#1399=EDGE_LOOP('',(#4379));
#1400=EDGE_LOOP('',(#4380,#4381,#4382,#4383,#4384,#4385));
#1401=EDGE_LOOP('',(#4386,#4387,#4388,#4389));
#1402=EDGE_LOOP('',(#4390,#4391,#4392,#4393));
#1403=EDGE_LOOP('',(#4394,#4395,#4396,#4397));
#1404=EDGE_LOOP('',(#4398));
#1729=LINE('',#8991,#2074);
#1730=LINE('',#8993,#2075);
#1731=LINE('',#8995,#2076);
#1732=LINE('',#8996,#2077);
#1733=LINE('',#8999,#2078);
#1734=LINE('',#9001,#2079);
#1735=LINE('',#9002,#2080);
#1736=LINE('',#9005,#2081);
#1737=LINE('',#9007,#2082);
#1738=LINE('',#9008,#2083);
#1739=LINE('',#9011,#2084);
#1740=LINE('',#9013,#2085);
#1741=LINE('',#9014,#2086);
#1742=LINE('',#9017,#2087);
#1743=LINE('',#9019,#2088);
#1744=LINE('',#9020,#2089);
#1745=LINE('',#9022,#2090);
#1746=LINE('',#9023,#2091);
#1747=LINE('',#9031,#2092);
#1748=LINE('',#9035,#2093);
#1749=LINE('',#9039,#2094);
#2074=VECTOR('',#6964,1.);
#2075=VECTOR('',#6965,1.);
#2076=VECTOR('',#6966,1.);
#2077=VECTOR('',#6967,1.);
#2078=VECTOR('',#6970,1.);
#2079=VECTOR('',#6971,1.);
#2080=VECTOR('',#6972,1.);
#2081=VECTOR('',#6975,1.);
#2082=VECTOR('',#6976,1.);
#2083=VECTOR('',#6977,1.);
#2084=VECTOR('',#6980,1.);
#2085=VECTOR('',#6981,1.);
#2086=VECTOR('',#6982,1.);
#2087=VECTOR('',#6985,1.);
#2088=VECTOR('',#6986,1.);
#2089=VECTOR('',#6987,1.);
#2090=VECTOR('',#6990,1.);
#2091=VECTOR('',#6991,1.);
#2092=VECTOR('',#7002,0.235);
#2093=VECTOR('',#7007,0.25);
#2094=VECTOR('',#7012,0.2125);
#2272=CIRCLE('',#5599,0.22);
#2273=CIRCLE('',#5601,0.24505);
#2274=CIRCLE('',#5603,0.24505);
#2275=CIRCLE('',#5605,0.175);
#2649=VERTEX_POINT('',#8989);
#2650=VERTEX_POINT('',#8990);
#2651=VERTEX_POINT('',#8992);
#2652=VERTEX_POINT('',#8994);
#2653=VERTEX_POINT('',#8998);
#2654=VERTEX_POINT('',#9000);
#2655=VERTEX_POINT('',#9004);
#2656=VERTEX_POINT('',#9006);
#2657=VERTEX_POINT('',#9010);
#2658=VERTEX_POINT('',#9012);
#2659=VERTEX_POINT('',#9016);
#2660=VERTEX_POINT('',#9018);
#2661=VERTEX_POINT('',#9026);
#2662=VERTEX_POINT('',#9029);
#2663=VERTEX_POINT('',#9033);
#2664=VERTEX_POINT('',#9037);
#3218=EDGE_CURVE('',#2649,#2650,#1729,.T.);
#3219=EDGE_CURVE('',#2649,#2651,#1730,.T.);
#3220=EDGE_CURVE('',#2651,#2652,#1731,.T.);
#3221=EDGE_CURVE('',#2650,#2652,#1732,.T.);
#3222=EDGE_CURVE('',#2653,#2649,#1733,.T.);
#3223=EDGE_CURVE('',#2653,#2654,#1734,.T.);
#3224=EDGE_CURVE('',#2654,#2651,#1735,.T.);
#3225=EDGE_CURVE('',#2655,#2653,#1736,.T.);
#3226=EDGE_CURVE('',#2655,#2656,#1737,.T.);
#3227=EDGE_CURVE('',#2656,#2654,#1738,.T.);
#3228=EDGE_CURVE('',#2657,#2655,#1739,.T.);
#3229=EDGE_CURVE('',#2657,#2658,#1740,.T.);
#3230=EDGE_CURVE('',#2658,#2656,#1741,.T.);
#3231=EDGE_CURVE('',#2659,#2657,#1742,.T.);
#3232=EDGE_CURVE('',#2659,#2660,#1743,.T.);
#3233=EDGE_CURVE('',#2660,#2658,#1744,.T.);
#3234=EDGE_CURVE('',#2650,#2659,#1745,.T.);
#3235=EDGE_CURVE('',#2652,#2660,#1746,.T.);
#3236=EDGE_CURVE('',#2661,#2661,#2272,.T.);
#3237=EDGE_CURVE('',#2662,#2662,#2273,.T.);
#3238=EDGE_CURVE('',#2662,#2661,#1747,.T.);
#3239=EDGE_CURVE('',#2663,#2663,#2274,.F.);
#3240=EDGE_CURVE('',#2663,#2662,#1748,.T.);
#3241=EDGE_CURVE('',#2664,#2664,#2275,.T.);
#3242=EDGE_CURVE('',#2664,#2663,#1749,.T.);
#4349=ORIENTED_EDGE('',*,*,#3218,.F.);
#4350=ORIENTED_EDGE('',*,*,#3219,.T.);
#4351=ORIENTED_EDGE('',*,*,#3220,.T.);
#4352=ORIENTED_EDGE('',*,*,#3221,.F.);
#4353=ORIENTED_EDGE('',*,*,#3222,.F.);
#4354=ORIENTED_EDGE('',*,*,#3223,.T.);
#4355=ORIENTED_EDGE('',*,*,#3224,.T.);
#4356=ORIENTED_EDGE('',*,*,#3219,.F.);
#4357=ORIENTED_EDGE('',*,*,#3225,.F.);
#4358=ORIENTED_EDGE('',*,*,#3226,.T.);
#4359=ORIENTED_EDGE('',*,*,#3227,.T.);
#4360=ORIENTED_EDGE('',*,*,#3223,.F.);
#4361=ORIENTED_EDGE('',*,*,#3228,.F.);
#4362=ORIENTED_EDGE('',*,*,#3229,.T.);
#4363=ORIENTED_EDGE('',*,*,#3230,.T.);
#4364=ORIENTED_EDGE('',*,*,#3226,.F.);
#4365=ORIENTED_EDGE('',*,*,#3231,.F.);
#4366=ORIENTED_EDGE('',*,*,#3232,.T.);
#4367=ORIENTED_EDGE('',*,*,#3233,.T.);
#4368=ORIENTED_EDGE('',*,*,#3229,.F.);
#4369=ORIENTED_EDGE('',*,*,#3234,.F.);
#4370=ORIENTED_EDGE('',*,*,#3221,.T.);
#4371=ORIENTED_EDGE('',*,*,#3235,.T.);
#4372=ORIENTED_EDGE('',*,*,#3232,.F.);
#4373=ORIENTED_EDGE('',*,*,#3235,.F.);
#4374=ORIENTED_EDGE('',*,*,#3220,.F.);
#4375=ORIENTED_EDGE('',*,*,#3224,.F.);
#4376=ORIENTED_EDGE('',*,*,#3227,.F.);
#4377=ORIENTED_EDGE('',*,*,#3230,.F.);
#4378=ORIENTED_EDGE('',*,*,#3233,.F.);
#4379=ORIENTED_EDGE('',*,*,#3236,.F.);
#4380=ORIENTED_EDGE('',*,*,#3218,.T.);
#4381=ORIENTED_EDGE('',*,*,#3234,.T.);
#4382=ORIENTED_EDGE('',*,*,#3231,.T.);
#4383=ORIENTED_EDGE('',*,*,#3228,.T.);
#4384=ORIENTED_EDGE('',*,*,#3225,.T.);
#4385=ORIENTED_EDGE('',*,*,#3222,.T.);
#4386=ORIENTED_EDGE('',*,*,#3237,.F.);
#4387=ORIENTED_EDGE('',*,*,#3238,.T.);
#4388=ORIENTED_EDGE('',*,*,#3236,.T.);
#4389=ORIENTED_EDGE('',*,*,#3238,.F.);
#4390=ORIENTED_EDGE('',*,*,#3239,.F.);
#4391=ORIENTED_EDGE('',*,*,#3240,.T.);
#4392=ORIENTED_EDGE('',*,*,#3237,.T.);
#4393=ORIENTED_EDGE('',*,*,#3240,.F.);
#4394=ORIENTED_EDGE('',*,*,#3241,.F.);
#4395=ORIENTED_EDGE('',*,*,#3242,.T.);
#4396=ORIENTED_EDGE('',*,*,#3239,.T.);
#4397=ORIENTED_EDGE('',*,*,#3242,.F.);
#4398=ORIENTED_EDGE('',*,*,#3241,.T.);
#4479=CYLINDRICAL_SURFACE('',#5602,0.24505);
#4740=ADVANCED_FACE('',(#1004),#735,.F.);
#4741=ADVANCED_FACE('',(#1005),#736,.F.);
#4742=ADVANCED_FACE('',(#1006),#737,.F.);
#4743=ADVANCED_FACE('',(#1007),#738,.F.);
#4744=ADVANCED_FACE('',(#1008),#739,.F.);
#4745=ADVANCED_FACE('',(#1009),#740,.F.);
#4746=ADVANCED_FACE('',(#1010),#741,.F.);
#4747=ADVANCED_FACE('',(#1011,#569),#742,.T.);
#4748=ADVANCED_FACE('',(#1012),#36,.T.);
#4749=ADVANCED_FACE('',(#1013),#4479,.T.);
#4750=ADVANCED_FACE('',(#1014),#37,.T.);
#4751=ADVANCED_FACE('',(#1015),#743,.T.);
#4783=CLOSED_SHELL('',(#4740,#4741,#4742,#4743,#4744,#4745,#4746,#4747,
#4748,#4749,#4750,#4751));
#5590=AXIS2_PLACEMENT_3D('',#8987,#6960,#6961);
#5591=AXIS2_PLACEMENT_3D('',#8988,#6962,#6963);
#5592=AXIS2_PLACEMENT_3D('',#8997,#6968,#6969);
#5593=AXIS2_PLACEMENT_3D('',#9003,#6973,#6974);
#5594=AXIS2_PLACEMENT_3D('',#9009,#6978,#6979);
#5595=AXIS2_PLACEMENT_3D('',#9015,#6983,#6984);
#5596=AXIS2_PLACEMENT_3D('',#9021,#6988,#6989);
#5597=AXIS2_PLACEMENT_3D('',#9024,#6992,#6993);
#5598=AXIS2_PLACEMENT_3D('',#9025,#6994,#6995);
#5599=AXIS2_PLACEMENT_3D('',#9027,#6996,#6997);
#5600=AXIS2_PLACEMENT_3D('',#9028,#6998,#6999);
#5601=AXIS2_PLACEMENT_3D('',#9030,#7000,#7001);
#5602=AXIS2_PLACEMENT_3D('',#9032,#7003,#7004);
#5603=AXIS2_PLACEMENT_3D('',#9034,#7005,#7006);
#5604=AXIS2_PLACEMENT_3D('',#9036,#7008,#7009);
#5605=AXIS2_PLACEMENT_3D('',#9038,#7010,#7011);
#5606=AXIS2_PLACEMENT_3D('',#9040,#7013,#7014);
#6960=DIRECTION('axis',(0.,0.,1.));
#6961=DIRECTION('refdir',(1.,0.,0.));
#6962=DIRECTION('center_axis',(0.866025403784439,0.,-0.5));
#6963=DIRECTION('ref_axis',(0.5,0.,0.866025403784439));
#6964=DIRECTION('',(0.5,0.,0.866025403784439));
#6965=DIRECTION('',(0.,-1.,0.));
#6966=DIRECTION('',(0.5,0.,0.866025403784439));
#6967=DIRECTION('',(0.,-1.,0.));
#6968=DIRECTION('center_axis',(1.92296268638356E-16,0.,-1.));
#6969=DIRECTION('ref_axis',(1.,0.,1.92296268638356E-16));
#6970=DIRECTION('',(1.,0.,1.92296268638356E-16));
#6971=DIRECTION('',(0.,-1.,0.));
#6972=DIRECTION('',(1.,0.,1.92296268638356E-16));
#6973=DIRECTION('center_axis',(-0.866025403784439,0.,-0.5));
#6974=DIRECTION('ref_axis',(0.5,0.,-0.866025403784439));
#6975=DIRECTION('',(0.5,0.,-0.866025403784439));
#6976=DIRECTION('',(0.,-1.,0.));
#6977=DIRECTION('',(0.5,0.,-0.866025403784438));
#6978=DIRECTION('center_axis',(-0.866025403784439,0.,0.5));
#6979=DIRECTION('ref_axis',(-0.5,0.,-0.866025403784439));
#6980=DIRECTION('',(-0.5,0.,-0.866025403784439));
#6981=DIRECTION('',(0.,-1.,0.));
#6982=DIRECTION('',(-0.5,0.,-0.866025403784439));
#6983=DIRECTION('center_axis',(-1.92296268638356E-16,0.,1.));
#6984=DIRECTION('ref_axis',(-1.,0.,-1.92296268638356E-16));
#6985=DIRECTION('',(-1.,0.,-1.92296268638356E-16));
#6986=DIRECTION('',(0.,-1.,0.));
#6987=DIRECTION('',(-1.,0.,-1.92296268638356E-16));
#6988=DIRECTION('center_axis',(0.866025403784439,0.,0.5));
#6989=DIRECTION('ref_axis',(-0.5,0.,0.866025403784439));
#6990=DIRECTION('',(-0.5,0.,0.866025403784439));
#6991=DIRECTION('',(-0.5,0.,0.866025403784439));
#6992=DIRECTION('center_axis',(0.,-1.,0.));
#6993=DIRECTION('ref_axis',(0.,0.,-1.));
#6994=DIRECTION('center_axis',(0.,1.,0.));
#6995=DIRECTION('ref_axis',(0.,0.,1.));
#6996=DIRECTION('center_axis',(0.,-1.,0.));
#6997=DIRECTION('ref_axis',(1.,0.,0.));
#6998=DIRECTION('center_axis',(0.,-1.,0.));
#6999=DIRECTION('ref_axis',(1.,0.,0.));
#7000=DIRECTION('center_axis',(0.,-1.,0.));
#7001=DIRECTION('ref_axis',(1.,0.,0.));
#7002=DIRECTION('',(0.707106781186547,0.707106781186548,8.65956056235493E-17));
#7003=DIRECTION('center_axis',(0.,-1.,0.));
#7004=DIRECTION('ref_axis',(1.,0.,0.));
#7005=DIRECTION('center_axis',(0.,1.,0.));
#7006=DIRECTION('ref_axis',(1.,0.,0.));
#7007=DIRECTION('',(0.,1.,0.));
#7008=DIRECTION('center_axis',(0.,1.,0.));
#7009=DIRECTION('ref_axis',(1.,0.,0.));
#7010=DIRECTION('center_axis',(0.,-1.,0.));
#7011=DIRECTION('ref_axis',(1.,0.,0.));
#7012=DIRECTION('',(-0.707106781186547,0.707106781186548,-8.65956056235493E-17));
#7013=DIRECTION('center_axis',(0.,-1.,0.));
#7014=DIRECTION('ref_axis',(0.,0.,-1.));
#8987=CARTESIAN_POINT('',(0.,0.,0.));
#8988=CARTESIAN_POINT('Origin',(0.0721687836487032,0.,-0.125));
#8989=CARTESIAN_POINT('',(0.0721687836487032,0.,-0.125));
#8990=CARTESIAN_POINT('',(0.144337567297406,0.,0.));
#8991=CARTESIAN_POINT('',(0.117710979560879,0.,-0.0461186027918559));
#8992=CARTESIAN_POINT('',(0.0721687836487032,-0.25,-0.125));
#8993=CARTESIAN_POINT('',(0.0721687836487032,0.,-0.125));
#8994=CARTESIAN_POINT('',(0.144337567297406,-0.25,0.));
#8995=CARTESIAN_POINT('',(0.144337567297406,-0.25,0.));
#8996=CARTESIAN_POINT('',(0.144337567297406,0.,0.));
#8997=CARTESIAN_POINT('Origin',(-0.0721687836487032,0.,-0.125));
#8998=CARTESIAN_POINT('',(-0.0721687836487032,0.,-0.125));
#8999=CARTESIAN_POINT('',(0.0739156081756484,0.,-0.125));
#9000=CARTESIAN_POINT('',(-0.0721687836487032,-0.25,-0.125));
#9001=CARTESIAN_POINT('',(-0.0721687836487032,0.,-0.125));
#9002=CARTESIAN_POINT('',(0.0721687836487032,-0.25,-0.125));
#9003=CARTESIAN_POINT('Origin',(-0.144337567297406,0.,-4.16333634234434E-17));
#9004=CARTESIAN_POINT('',(-0.144337567297406,0.,-1.76762539787485E-17));
#9005=CARTESIAN_POINT('',(-0.0987953713852306,0.,-0.0788813972081442));
#9006=CARTESIAN_POINT('',(-0.144337567297406,-0.25,-2.77555756156289E-17));
#9007=CARTESIAN_POINT('',(-0.144337567297406,0.,-1.76762539787485E-17));
#9008=CARTESIAN_POINT('',(-0.0721687836487032,-0.25,-0.125));
#9009=CARTESIAN_POINT('Origin',(-0.0721687836487033,0.,0.125));
#9010=CARTESIAN_POINT('',(-0.0721687836487033,0.,0.125));
#9011=CARTESIAN_POINT('',(-0.0627109795608791,0.,0.141381397208144));
#9012=CARTESIAN_POINT('',(-0.0721687836487033,-0.25,0.125));
#9013=CARTESIAN_POINT('',(-0.0721687836487033,0.,0.125));
#9014=CARTESIAN_POINT('',(-0.144337567297406,-0.25,-1.76762539787485E-17));
#9015=CARTESIAN_POINT('Origin',(0.0721687836487032,0.,0.125));
#9016=CARTESIAN_POINT('',(0.0721687836487032,0.,0.125));
#9017=CARTESIAN_POINT('',(0.146084391824352,0.,0.125));
#9018=CARTESIAN_POINT('',(0.0721687836487032,-0.25,0.125));
#9019=CARTESIAN_POINT('',(0.0721687836487032,0.,0.125));
#9020=CARTESIAN_POINT('',(-0.0721687836487033,-0.25,0.125));
#9021=CARTESIAN_POINT('Origin',(0.144337567297406,0.,0.));
#9022=CARTESIAN_POINT('',(0.153795371385231,0.,-0.0163813972081441));
#9023=CARTESIAN_POINT('',(0.0721687836487032,-0.25,0.125));
#9024=CARTESIAN_POINT('Origin',(0.,-0.25,0.));
#9025=CARTESIAN_POINT('Origin',(0.22,0.,0.));
#9026=CARTESIAN_POINT('',(-0.22,-8.67361737988404E-18,-2.69422295812418E-17));
#9027=CARTESIAN_POINT('Origin',(0.,0.,0.));
#9028=CARTESIAN_POINT('Origin',(0.,-0.015,0.));
#9029=CARTESIAN_POINT('',(-0.24505,-0.02505,-3.00099698131059E-17));
#9030=CARTESIAN_POINT('Origin',(0.,-0.02505,0.));
#9031=CARTESIAN_POINT('',(-0.235,-0.015,-2.87791997799628E-17));
#9032=CARTESIAN_POINT('Origin',(0.,-0.3775,0.));
#9033=CARTESIAN_POINT('',(-0.24505,-0.72995,3.00099698131059E-17));
#9034=CARTESIAN_POINT('Origin',(0.,-0.72995,0.));
#9035=CARTESIAN_POINT('',(-0.24505,-0.3775,-3.00099698131059E-17));
#9036=CARTESIAN_POINT('Origin',(0.,-0.7625,0.));
#9037=CARTESIAN_POINT('',(-0.175,-0.8,-2.14313189850787E-17));
#9038=CARTESIAN_POINT('Origin',(0.,-0.8,0.));
#9039=CARTESIAN_POINT('',(-0.2125,-0.7625,-2.60237444818813E-17));
#9040=CARTESIAN_POINT('Origin',(0.,-0.8,0.));
#9107=UNCERTAINTY_MEASURE_WITH_UNIT(LENGTH_MEASURE(0.001),#9142,
'DISTANCE_ACCURACY_VALUE',
'Maximum model space distance between geometric entities at asserted c
onnectivities');
#9108=UNCERTAINTY_MEASURE_WITH_UNIT(LENGTH_MEASURE(0.001),#9142,
'DISTANCE_ACCURACY_VALUE',
'Maximum model space distance between geometric entities at asserted c
onnectivities');
#9140=(
GEOMETRIC_REPRESENTATION_CONTEXT(3)
GLOBAL_UNCERTAINTY_ASSIGNED_CONTEXT((#9107))
GLOBAL_UNIT_ASSIGNED_CONTEXT((#9142,#9144,#9145))
REPRESENTATION_CONTEXT('','3D')
);
#9141=(
GEOMETRIC_REPRESENTATION_CONTEXT(3)
GLOBAL_UNCERTAINTY_ASSIGNED_CONTEXT((#9108))
GLOBAL_UNIT_ASSIGNED_CONTEXT((#9142,#9144,#9145))
REPRESENTATION_CONTEXT('','3D')
);
#9142=(
LENGTH_UNIT()
NAMED_UNIT(*)
SI_UNIT(.CENTI.,.METRE.)
);
#9144=(
NAMED_UNIT(*)
PLANE_ANGLE_UNIT()
SI_UNIT($,.RADIAN.)
);
#9145=(
NAMED_UNIT(*)
SI_UNIT($,.STERADIAN.)
SOLID_ANGLE_UNIT()
);
#9177=SHAPE_DEFINITION_REPRESENTATION(#9238,#9305);
#9238=PRODUCT_DEFINITION_SHAPE('',$,#9338);
#9305=SHAPE_REPRESENTATION('',(#5590),#9140);
#9306=PRODUCT_DEFINITION_CONTEXT('part definition',#9404,'design');
#9338=PRODUCT_DEFINITION('Socket Set Screw - M5x8',
'Socket Set Screw - M5x8',#9370,#9306);
#9370=PRODUCT_DEFINITION_FORMATION('',$,#9437);
#9404=APPLICATION_CONTEXT(
'Core Data for Automotive Mechanical Design Process');
#9405=PRODUCT_CONTEXT('part definition',#9404,'mechanical');
#9437=PRODUCT('Socket Set Screw - M5x8','Socket Set Screw - M5x8',
'Socket Set Screw - M5x8',(#9405));
#9501=COLOUR_RGB('Black',0.12,0.14,0.17);
#9502=FILL_AREA_STYLE_COLOUR('',#9501);
#9503=FILL_AREA_STYLE('',(#9502));
#9504=SURFACE_STYLE_FILL_AREA(#9503);
#9505=SURFACE_SIDE_STYLE('',(#9504));
#9506=SURFACE_STYLE_USAGE(.BOTH.,#9505);
#9507=PRESENTATION_STYLE_ASSIGNMENT((#9506));
ENDSEC;
END-ISO-10303-21;
